ISO-10303-21;
HEADER;
/* Generated by software containing ST-Developer
 * from STEP Tools, Inc. (www.steptools.com) 
 */

FILE_DESCRIPTION(
/* description */ ('Independent30mm screw-fed quill/spindle unit with16mm straight tool s
ocket, radial set screw, native reusable open ball bearings, retained 
inner/outer race stacks, keyed quill guide and M12x1.75 fine feed. Ext
ernal moving drive and tool not included. Ideal cage orbital links; in
dividual ball spin, force and preload not simulated. No drilling capac
ity, runout, speed, torque, load, life or machine safety rating.'),
/* implementation_level */ '2;1');

FILE_NAME(
/* name */ 'Spindle thrust washer.step',
/* time_stamp */ '2026-11-08T18:59:42-08:00',
/* author */ (''),
/* organization */ (''),
/* preprocessor_version */ 'ST-DEVELOPER v20.2',
/* originating_system */ 'Autodesk Translation Framework v15.17.0.0',
/* authorisation */ '');

FILE_SCHEMA (('AUTOMOTIVE_DESIGN { 1 0 10303 214 3 1 1 }'));
ENDSEC;

DATA;
#10=MECHANICAL_DESIGN_GEOMETRIC_PRESENTATION_REPRESENTATION('',(#1596),#63898);
#1560=SHAPE_REPRESENTATION_RELATIONSHIP('SRR','None',#63999,#1578);
#1578=ADVANCED_BREP_SHAPE_REPRESENTATION('',(#1614),#63884);
#1596=STYLED_ITEM('',(#64098),#1614);
#1614=MANIFOLD_SOLID_BREP('Body1',#15482);
#1671=FACE_BOUND('',#4018,.T.);
#1672=FACE_BOUND('',#4020,.T.);
#2108=CYLINDRICAL_SURFACE('',#16278,20.);
#2109=CYLINDRICAL_SURFACE('',#16281,27.5);
#2503=CIRCLE('',#16279,20.);
#2504=CIRCLE('',#16280,20.);
#2505=CIRCLE('',#16282,27.5);
#2506=CIRCLE('',#16283,27.5);
#3134=FACE_OUTER_BOUND('',#4015,.T.);
#3135=FACE_OUTER_BOUND('',#4016,.T.);
#3136=FACE_OUTER_BOUND('',#4017,.T.);
#3137=FACE_OUTER_BOUND('',#4019,.T.);
#4015=EDGE_LOOP('',(#12508,#12509,#12510,#12511));
#4016=EDGE_LOOP('',(#12512,#12513,#12514,#12515));
#4017=EDGE_LOOP('',(#12516));
#4018=EDGE_LOOP('',(#12517));
#4019=EDGE_LOOP('',(#12518));
#4020=EDGE_LOOP('',(#12519));
#4858=LINE('',#46775,#5621);
#4859=LINE('',#46781,#5622);
#5621=VECTOR('',#18464,20.);
#5622=VECTOR('',#18471,27.5);
#6836=VERTEX_POINT('',#46772);
#6837=VERTEX_POINT('',#46774);
#6838=VERTEX_POINT('',#46778);
#6839=VERTEX_POINT('',#46780);
#8843=EDGE_CURVE('',#6836,#6836,#2503,.T.);
#8844=EDGE_CURVE('',#6836,#6837,#4858,.T.);
#8845=EDGE_CURVE('',#6837,#6837,#2504,.T.);
#8846=EDGE_CURVE('',#6838,#6838,#2505,.T.);
#8847=EDGE_CURVE('',#6838,#6839,#4859,.T.);
#8848=EDGE_CURVE('',#6839,#6839,#2506,.T.);
#12508=ORIENTED_EDGE('',*,*,#8843,.F.);
#12509=ORIENTED_EDGE('',*,*,#8844,.T.);
#12510=ORIENTED_EDGE('',*,*,#8845,.T.);
#12511=ORIENTED_EDGE('',*,*,#8844,.F.);
#12512=ORIENTED_EDGE('',*,*,#8846,.F.);
#12513=ORIENTED_EDGE('',*,*,#8847,.T.);
#12514=ORIENTED_EDGE('',*,*,#8848,.T.);
#12515=ORIENTED_EDGE('',*,*,#8847,.F.);
#12516=ORIENTED_EDGE('',*,*,#8846,.T.);
#12517=ORIENTED_EDGE('',*,*,#8843,.T.);
#12518=ORIENTED_EDGE('',*,*,#8848,.F.);
#12519=ORIENTED_EDGE('',*,*,#8845,.F.);
#14571=PLANE('',#16284);
#14572=PLANE('',#16285);
#15114=ADVANCED_FACE('',(#3134),#2108,.F.);
#15115=ADVANCED_FACE('',(#3135),#2109,.T.);
#15116=ADVANCED_FACE('',(#3136,#1671),#14571,.T.);
#15117=ADVANCED_FACE('',(#3137,#1672),#14572,.F.);
#15482=CLOSED_SHELL('',(#15114,#15115,#15116,#15117));
#16277=AXIS2_PLACEMENT_3D('',#46770,#18458,#18459);
#16278=AXIS2_PLACEMENT_3D('',#46771,#18460,#18461);
#16279=AXIS2_PLACEMENT_3D('',#46773,#18462,#18463);
#16280=AXIS2_PLACEMENT_3D('',#46776,#18465,#18466);
#16281=AXIS2_PLACEMENT_3D('',#46777,#18467,#18468);
#16282=AXIS2_PLACEMENT_3D('',#46779,#18469,#18470);
#16283=AXIS2_PLACEMENT_3D('',#46782,#18472,#18473);
#16284=AXIS2_PLACEMENT_3D('',#46783,#18474,#18475);
#16285=AXIS2_PLACEMENT_3D('',#46784,#18476,#18477);
#18458=DIRECTION('axis',(0.,0.,1.));
#18459=DIRECTION('refdir',(1.,0.,0.));
#18460=DIRECTION('center_axis',(0.,0.,1.));
#18461=DIRECTION('ref_axis',(1.,0.,0.));
#18462=DIRECTION('center_axis',(0.,0.,-1.));
#18463=DIRECTION('ref_axis',(1.,0.,0.));
#18464=DIRECTION('',(0.,0.,-1.));
#18465=DIRECTION('center_axis',(0.,0.,-1.));
#18466=DIRECTION('ref_axis',(1.,0.,0.));
#18467=DIRECTION('center_axis',(0.,0.,1.));
#18468=DIRECTION('ref_axis',(1.,0.,0.));
#18469=DIRECTION('center_axis',(0.,0.,1.));
#18470=DIRECTION('ref_axis',(1.,0.,0.));
#18471=DIRECTION('',(0.,0.,-1.));
#18472=DIRECTION('center_axis',(0.,0.,1.));
#18473=DIRECTION('ref_axis',(1.,0.,0.));
#18474=DIRECTION('center_axis',(0.,0.,1.));
#18475=DIRECTION('ref_axis',(1.,0.,0.));
#18476=DIRECTION('center_axis',(0.,0.,1.));
#18477=DIRECTION('ref_axis',(1.,0.,0.));
#46770=CARTESIAN_POINT('',(0.,0.,0.));
#46771=CARTESIAN_POINT('Origin',(0.,0.,179.));
#46772=CARTESIAN_POINT('',(-20.,-2.44929359829471E-15,181.));
#46773=CARTESIAN_POINT('Origin',(0.,0.,181.));
#46774=CARTESIAN_POINT('',(-20.,-2.44929359829471E-15,179.));
#46775=CARTESIAN_POINT('',(-20.,-2.44929359829471E-15,179.));
#46776=CARTESIAN_POINT('Origin',(0.,0.,179.));
#46777=CARTESIAN_POINT('Origin',(0.,0.,179.));
#46778=CARTESIAN_POINT('',(-27.5,-3.36777869765522E-15,181.));
#46779=CARTESIAN_POINT('Origin',(0.,0.,181.));
#46780=CARTESIAN_POINT('',(-27.5,-3.36777869765522E-15,179.));
#46781=CARTESIAN_POINT('',(-27.5,-3.36777869765522E-15,179.));
#46782=CARTESIAN_POINT('Origin',(0.,0.,179.));
#46783=CARTESIAN_POINT('Origin',(0.,0.,181.));
#46784=CARTESIAN_POINT('Origin',(0.,0.,179.));
#63864=UNCERTAINTY_MEASURE_WITH_UNIT(LENGTH_MEASURE(0.01),#63899,
'DISTANCE_ACCURACY_VALUE',
'Maximum model space distance between geometric entities at asserted c
onnectivities');
#63878=UNCERTAINTY_MEASURE_WITH_UNIT(LENGTH_MEASURE(0.01),#63899,
'DISTANCE_ACCURACY_VALUE',
'Maximum model space distance between geometric entities at asserted c
onnectivities');
#63884=(
GEOMETRIC_REPRESENTATION_CONTEXT(3)
GLOBAL_UNCERTAINTY_ASSIGNED_CONTEXT((#63864))
GLOBAL_UNIT_ASSIGNED_CONTEXT((#63899,#63901,#63902))
REPRESENTATION_CONTEXT('','3D')
);
#63898=(
GEOMETRIC_REPRESENTATION_CONTEXT(3)
GLOBAL_UNCERTAINTY_ASSIGNED_CONTEXT((#63878))
GLOBAL_UNIT_ASSIGNED_CONTEXT((#63899,#63901,#63902))
REPRESENTATION_CONTEXT('','3D')
);
#63899=(
LENGTH_UNIT()
NAMED_UNIT(*)
SI_UNIT(.MILLI.,.METRE.)
);
#63901=(
NAMED_UNIT(*)
PLANE_ANGLE_UNIT()
SI_UNIT($,.RADIAN.)
);
#63902=(
NAMED_UNIT(*)
SI_UNIT($,.STERADIAN.)
SOLID_ANGLE_UNIT()
);
#63908=SHAPE_DEFINITION_REPRESENTATION(#63927,#63999);
#63927=PRODUCT_DEFINITION_SHAPE('',$,#64019);
#63999=SHAPE_REPRESENTATION('',(#16277),#63884);
#64013=PRODUCT_DEFINITION_CONTEXT('part definition',#64072,'design');
#64019=PRODUCT_DEFINITION('Spindle thrust washer',
'Spindle thrust washer',#64038,#64013);
#64038=PRODUCT_DEFINITION_FORMATION('',$,#64079);
#64072=APPLICATION_CONTEXT(
'Core Data for Automotive Mechanical Design Process');
#64073=PRODUCT_CONTEXT('part definition',#64072,'mechanical');
#64079=PRODUCT('Spindle thrust washer','Spindle thrust washer',$,(#64073));
#64098=PRESENTATION_STYLE_ASSIGNMENT((#64111));
#64111=SURFACE_STYLE_USAGE(.BOTH.,#64124);
#64124=SURFACE_SIDE_STYLE('',(#64137));
#64137=SURFACE_STYLE_FILL_AREA(#64150);
#64150=FILL_AREA_STYLE('Gray',(#64163));
#64163=FILL_AREA_STYLE_COLOUR('Gray',#64176);
#64176=COLOUR_RGB('Gray',0.407843137254902,0.447058823529412,0.498039215686275);
ENDSEC;
END-ISO-10303-21;
